ISO-10303-21;
HEADER;
/* Generated by software containing ST-Developer
 * from STEP Tools, Inc. (www.steptools.com) 
 */

FILE_DESCRIPTION(
/* description */ ('Bin tilter linkage'),
/* implementation_level */ '2;1');

FILE_NAME(
/* name */ 'Screw bearing keeper (3).step',
/* time_stamp */ '2026-10-28T03:26:24-07:00',
/* author */ (''),
/* organization */ (''),
/* preprocessor_version */ 'ST-DEVELOPER v20.2',
/* originating_system */ 'Autodesk Translation Framework v15.17.0.0',
/* authorisation */ '');

FILE_SCHEMA (('AUTOMOTIVE_DESIGN { 1 0 10303 214 3 1 1 }'));
ENDSEC;

DATA;
#10=MECHANICAL_DESIGN_GEOMETRIC_PRESENTATION_REPRESENTATION('',(#886),#23728);
#674=SHAPE_REPRESENTATION_RELATIONSHIP('SRR','None',#24138,#780);
#780=ADVANCED_BREP_SHAPE_REPRESENTATION('',(#1000),#23638);
#886=STYLED_ITEM('',(#24772),#1000);
#1000=MANIFOLD_SOLID_BREP('Body1',#12416);
#1225=FACE_BOUND('',#3017,.T.);
#1226=FACE_BOUND('',#3018,.T.);
#1227=FACE_BOUND('',#3019,.T.);
#1228=FACE_BOUND('',#3024,.T.);
#1229=FACE_BOUND('',#3025,.T.);
#1230=FACE_BOUND('',#3026,.T.);
#1594=PLANE('',#14132);
#1595=PLANE('',#14142);
#2097=FACE_OUTER_BOUND('',#3012,.T.);
#2098=FACE_OUTER_BOUND('',#3013,.T.);
#2099=FACE_OUTER_BOUND('',#3014,.T.);
#2100=FACE_OUTER_BOUND('',#3015,.T.);
#2101=FACE_OUTER_BOUND('',#3016,.T.);
#2102=FACE_OUTER_BOUND('',#3020,.T.);
#2103=FACE_OUTER_BOUND('',#3021,.T.);
#2104=FACE_OUTER_BOUND('',#3022,.T.);
#2105=FACE_OUTER_BOUND('',#3023,.T.);
#3012=EDGE_LOOP('',(#9231,#9232,#9233,#9234));
#3013=EDGE_LOOP('',(#9235,#9236,#9237,#9238));
#3014=EDGE_LOOP('',(#9239,#9240,#9241,#9242));
#3015=EDGE_LOOP('',(#9243,#9244,#9245,#9246));
#3016=EDGE_LOOP('',(#9247,#9248,#9249,#9250));
#3017=EDGE_LOOP('',(#9251));
#3018=EDGE_LOOP('',(#9252));
#3019=EDGE_LOOP('',(#9253));
#3020=EDGE_LOOP('',(#9254,#9255,#9256,#9257));
#3021=EDGE_LOOP('',(#9258,#9259,#9260,#9261));
#3022=EDGE_LOOP('',(#9262,#9263,#9264,#9265));
#3023=EDGE_LOOP('',(#9266,#9267,#9268,#9269));
#3024=EDGE_LOOP('',(#9270));
#3025=EDGE_LOOP('',(#9271));
#3026=EDGE_LOOP('',(#9272));
#4068=LINE('',#20698,#4743);
#4069=LINE('',#20704,#4744);
#4070=LINE('',#20709,#4745);
#4071=LINE('',#20713,#4746);
#4072=LINE('',#20718,#4747);
#4073=LINE('',#20722,#4748);
#4074=LINE('',#20735,#4749);
#4743=VECTOR('',#16585,0.225);
#4744=VECTOR('',#16592,0.225);
#4745=VECTOR('',#16597,1.);
#4746=VECTOR('',#16600,1.);
#4747=VECTOR('',#16605,1.);
#4748=VECTOR('',#16608,1.);
#4749=VECTOR('',#16629,1.02);
#5409=CIRCLE('',#14121,0.225);
#5410=CIRCLE('',#14122,0.225);
#5411=CIRCLE('',#14124,0.225);
#5412=CIRCLE('',#14125,0.225);
#5413=CIRCLE('',#14127,0.61);
#5414=CIRCLE('',#14128,0.61);
#5415=CIRCLE('',#14130,0.61);
#5416=CIRCLE('',#14131,0.61);
#5417=CIRCLE('',#14133,2.1);
#5418=CIRCLE('',#14134,2.1);
#5419=CIRCLE('',#14135,1.02);
#5420=CIRCLE('',#14137,2.1);
#5421=CIRCLE('',#14139,2.1);
#5422=CIRCLE('',#14141,1.02);
#6243=VERTEX_POINT('',#20695);
#6244=VERTEX_POINT('',#20697);
#6245=VERTEX_POINT('',#20701);
#6246=VERTEX_POINT('',#20703);
#6247=VERTEX_POINT('',#20707);
#6248=VERTEX_POINT('',#20708);
#6249=VERTEX_POINT('',#20710);
#6250=VERTEX_POINT('',#20712);
#6251=VERTEX_POINT('',#20716);
#6252=VERTEX_POINT('',#20717);
#6253=VERTEX_POINT('',#20719);
#6254=VERTEX_POINT('',#20721);
#6255=VERTEX_POINT('',#20727);
#6256=VERTEX_POINT('',#20734);
#7355=EDGE_CURVE('',#6243,#6243,#5409,.T.);
#7356=EDGE_CURVE('',#6243,#6244,#4068,.T.);
#7357=EDGE_CURVE('',#6244,#6244,#5410,.T.);
#7358=EDGE_CURVE('',#6245,#6245,#5411,.T.);
#7359=EDGE_CURVE('',#6245,#6246,#4069,.T.);
#7360=EDGE_CURVE('',#6246,#6246,#5412,.T.);
#7361=EDGE_CURVE('',#6247,#6248,#4070,.T.);
#7362=EDGE_CURVE('',#6249,#6247,#5413,.T.);
#7363=EDGE_CURVE('',#6250,#6249,#4071,.T.);
#7364=EDGE_CURVE('',#6248,#6250,#5414,.T.);
#7365=EDGE_CURVE('',#6251,#6252,#4072,.T.);
#7366=EDGE_CURVE('',#6253,#6251,#5415,.T.);
#7367=EDGE_CURVE('',#6254,#6253,#4073,.T.);
#7368=EDGE_CURVE('',#6252,#6254,#5416,.T.);
#7369=EDGE_CURVE('',#6247,#6253,#5417,.T.);
#7370=EDGE_CURVE('',#6251,#6249,#5418,.T.);
#7371=EDGE_CURVE('',#6255,#6255,#5419,.T.);
#7372=EDGE_CURVE('',#6248,#6254,#5420,.T.);
#7373=EDGE_CURVE('',#6252,#6250,#5421,.T.);
#7374=EDGE_CURVE('',#6255,#6256,#4074,.T.);
#7375=EDGE_CURVE('',#6256,#6256,#5422,.T.);
#9231=ORIENTED_EDGE('',*,*,#7355,.F.);
#9232=ORIENTED_EDGE('',*,*,#7356,.T.);
#9233=ORIENTED_EDGE('',*,*,#7357,.F.);
#9234=ORIENTED_EDGE('',*,*,#7356,.F.);
#9235=ORIENTED_EDGE('',*,*,#7358,.F.);
#9236=ORIENTED_EDGE('',*,*,#7359,.T.);
#9237=ORIENTED_EDGE('',*,*,#7360,.F.);
#9238=ORIENTED_EDGE('',*,*,#7359,.F.);
#9239=ORIENTED_EDGE('',*,*,#7361,.F.);
#9240=ORIENTED_EDGE('',*,*,#7362,.F.);
#9241=ORIENTED_EDGE('',*,*,#7363,.F.);
#9242=ORIENTED_EDGE('',*,*,#7364,.F.);
#9243=ORIENTED_EDGE('',*,*,#7365,.F.);
#9244=ORIENTED_EDGE('',*,*,#7366,.F.);
#9245=ORIENTED_EDGE('',*,*,#7367,.F.);
#9246=ORIENTED_EDGE('',*,*,#7368,.F.);
#9247=ORIENTED_EDGE('',*,*,#7362,.T.);
#9248=ORIENTED_EDGE('',*,*,#7369,.T.);
#9249=ORIENTED_EDGE('',*,*,#7366,.T.);
#9250=ORIENTED_EDGE('',*,*,#7370,.T.);
#9251=ORIENTED_EDGE('',*,*,#7357,.T.);
#9252=ORIENTED_EDGE('',*,*,#7360,.T.);
#9253=ORIENTED_EDGE('',*,*,#7371,.T.);
#9254=ORIENTED_EDGE('',*,*,#7361,.T.);
#9255=ORIENTED_EDGE('',*,*,#7372,.T.);
#9256=ORIENTED_EDGE('',*,*,#7367,.T.);
#9257=ORIENTED_EDGE('',*,*,#7369,.F.);
#9258=ORIENTED_EDGE('',*,*,#7363,.T.);
#9259=ORIENTED_EDGE('',*,*,#7370,.F.);
#9260=ORIENTED_EDGE('',*,*,#7365,.T.);
#9261=ORIENTED_EDGE('',*,*,#7373,.T.);
#9262=ORIENTED_EDGE('',*,*,#7371,.F.);
#9263=ORIENTED_EDGE('',*,*,#7374,.T.);
#9264=ORIENTED_EDGE('',*,*,#7375,.T.);
#9265=ORIENTED_EDGE('',*,*,#7374,.F.);
#9266=ORIENTED_EDGE('',*,*,#7364,.T.);
#9267=ORIENTED_EDGE('',*,*,#7373,.F.);
#9268=ORIENTED_EDGE('',*,*,#7368,.T.);
#9269=ORIENTED_EDGE('',*,*,#7372,.F.);
#9270=ORIENTED_EDGE('',*,*,#7355,.T.);
#9271=ORIENTED_EDGE('',*,*,#7358,.T.);
#9272=ORIENTED_EDGE('',*,*,#7375,.F.);
#11372=CYLINDRICAL_SURFACE('',#14120,0.225);
#11373=CYLINDRICAL_SURFACE('',#14123,0.225);
#11374=CYLINDRICAL_SURFACE('',#14126,0.61);
#11375=CYLINDRICAL_SURFACE('',#14129,0.61);
#11376=CYLINDRICAL_SURFACE('',#14136,2.1);
#11377=CYLINDRICAL_SURFACE('',#14138,2.1);
#11378=CYLINDRICAL_SURFACE('',#14140,1.02);
#11822=ADVANCED_FACE('',(#2097),#11372,.F.);
#11823=ADVANCED_FACE('',(#2098),#11373,.F.);
#11824=ADVANCED_FACE('',(#2099),#11374,.F.);
#11825=ADVANCED_FACE('',(#2100),#11375,.F.);
#11826=ADVANCED_FACE('',(#2101,#1225,#1226,#1227),#1594,.T.);
#11827=ADVANCED_FACE('',(#2102),#11376,.T.);
#11828=ADVANCED_FACE('',(#2103),#11377,.T.);
#11829=ADVANCED_FACE('',(#2104),#11378,.F.);
#11830=ADVANCED_FACE('',(#2105,#1228,#1229,#1230),#1595,.F.);
#12416=CLOSED_SHELL('',(#11822,#11823,#11824,#11825,#11826,#11827,#11828,
#11829,#11830));
#14119=AXIS2_PLACEMENT_3D('',#20693,#16579,#16580);
#14120=AXIS2_PLACEMENT_3D('',#20694,#16581,#16582);
#14121=AXIS2_PLACEMENT_3D('',#20696,#16583,#16584);
#14122=AXIS2_PLACEMENT_3D('',#20699,#16586,#16587);
#14123=AXIS2_PLACEMENT_3D('',#20700,#16588,#16589);
#14124=AXIS2_PLACEMENT_3D('',#20702,#16590,#16591);
#14125=AXIS2_PLACEMENT_3D('',#20705,#16593,#16594);
#14126=AXIS2_PLACEMENT_3D('',#20706,#16595,#16596);
#14127=AXIS2_PLACEMENT_3D('',#20711,#16598,#16599);
#14128=AXIS2_PLACEMENT_3D('',#20714,#16601,#16602);
#14129=AXIS2_PLACEMENT_3D('',#20715,#16603,#16604);
#14130=AXIS2_PLACEMENT_3D('',#20720,#16606,#16607);
#14131=AXIS2_PLACEMENT_3D('',#20723,#16609,#16610);
#14132=AXIS2_PLACEMENT_3D('',#20724,#16611,#16612);
#14133=AXIS2_PLACEMENT_3D('',#20725,#16613,#16614);
#14134=AXIS2_PLACEMENT_3D('',#20726,#16615,#16616);
#14135=AXIS2_PLACEMENT_3D('',#20728,#16617,#16618);
#14136=AXIS2_PLACEMENT_3D('',#20729,#16619,#16620);
#14137=AXIS2_PLACEMENT_3D('',#20730,#16621,#16622);
#14138=AXIS2_PLACEMENT_3D('',#20731,#16623,#16624);
#14139=AXIS2_PLACEMENT_3D('',#20732,#16625,#16626);
#14140=AXIS2_PLACEMENT_3D('',#20733,#16627,#16628);
#14141=AXIS2_PLACEMENT_3D('',#20736,#16630,#16631);
#14142=AXIS2_PLACEMENT_3D('',#20737,#16632,#16633);
#16579=DIRECTION('axis',(0.,0.,1.));
#16580=DIRECTION('refdir',(1.,0.,0.));
#16581=DIRECTION('center_axis',(1.,0.,0.));
#16582=DIRECTION('ref_axis',(0.,0.,-1.));
#16583=DIRECTION('center_axis',(1.,0.,0.));
#16584=DIRECTION('ref_axis',(0.,0.,-1.));
#16585=DIRECTION('',(1.,0.,0.));
#16586=DIRECTION('center_axis',(-1.,0.,0.));
#16587=DIRECTION('ref_axis',(0.,0.,-1.));
#16588=DIRECTION('center_axis',(1.,0.,0.));
#16589=DIRECTION('ref_axis',(0.,0.,-1.));
#16590=DIRECTION('center_axis',(1.,0.,0.));
#16591=DIRECTION('ref_axis',(0.,0.,-1.));
#16592=DIRECTION('',(1.,0.,0.));
#16593=DIRECTION('center_axis',(-1.,0.,0.));
#16594=DIRECTION('ref_axis',(0.,0.,-1.));
#16595=DIRECTION('center_axis',(1.,0.,0.));
#16596=DIRECTION('ref_axis',(0.,0.,-1.));
#16597=DIRECTION('',(-1.,0.,0.));
#16598=DIRECTION('center_axis',(-1.,0.,0.));
#16599=DIRECTION('ref_axis',(0.,0.,-1.));
#16600=DIRECTION('',(1.,0.,0.));
#16601=DIRECTION('center_axis',(1.,0.,0.));
#16602=DIRECTION('ref_axis',(0.,0.,-1.));
#16603=DIRECTION('center_axis',(1.,0.,0.));
#16604=DIRECTION('ref_axis',(0.,0.,-1.));
#16605=DIRECTION('',(-1.,0.,0.));
#16606=DIRECTION('center_axis',(-1.,0.,0.));
#16607=DIRECTION('ref_axis',(0.,0.,-1.));
#16608=DIRECTION('',(1.,0.,0.));
#16609=DIRECTION('center_axis',(1.,0.,0.));
#16610=DIRECTION('ref_axis',(0.,0.,-1.));
#16611=DIRECTION('center_axis',(1.,0.,0.));
#16612=DIRECTION('ref_axis',(0.,0.,-1.));
#16613=DIRECTION('center_axis',(1.,0.,0.));
#16614=DIRECTION('ref_axis',(0.,0.,-1.));
#16615=DIRECTION('center_axis',(1.,0.,0.));
#16616=DIRECTION('ref_axis',(0.,0.,-1.));
#16617=DIRECTION('center_axis',(-1.,0.,0.));
#16618=DIRECTION('ref_axis',(0.,0.,-1.));
#16619=DIRECTION('center_axis',(1.,0.,0.));
#16620=DIRECTION('ref_axis',(0.,0.,-1.));
#16621=DIRECTION('center_axis',(1.,0.,0.));
#16622=DIRECTION('ref_axis',(0.,0.,-1.));
#16623=DIRECTION('center_axis',(1.,0.,0.));
#16624=DIRECTION('ref_axis',(0.,-1.22464679914735E-16,1.));
#16625=DIRECTION('center_axis',(1.,0.,0.));
#16626=DIRECTION('ref_axis',(0.,0.,-1.));
#16627=DIRECTION('center_axis',(1.,0.,0.));
#16628=DIRECTION('ref_axis',(0.,0.,-1.));
#16629=DIRECTION('',(-1.,0.,0.));
#16630=DIRECTION('center_axis',(-1.,0.,0.));
#16631=DIRECTION('ref_axis',(0.,0.,-1.));
#16632=DIRECTION('center_axis',(1.,0.,0.));
#16633=DIRECTION('ref_axis',(0.,0.,-1.));
#20693=CARTESIAN_POINT('',(0.,0.,0.));
#20694=CARTESIAN_POINT('Origin',(0.9,-4.5,9.85));
#20695=CARTESIAN_POINT('',(1.,-4.5,10.075));
#20696=CARTESIAN_POINT('Origin',(1.,-4.5,9.85));
#20697=CARTESIAN_POINT('',(1.2,-4.5,10.075));
#20698=CARTESIAN_POINT('',(0.9,-4.5,10.075));
#20699=CARTESIAN_POINT('Origin',(1.2,-4.5,9.85));
#20700=CARTESIAN_POINT('Origin',(0.9,-4.5,6.15));
#20701=CARTESIAN_POINT('',(1.,-4.5,6.375));
#20702=CARTESIAN_POINT('Origin',(1.,-4.5,6.15));
#20703=CARTESIAN_POINT('',(1.2,-4.5,6.375));
#20704=CARTESIAN_POINT('',(0.9,-4.5,6.375));
#20705=CARTESIAN_POINT('Origin',(1.2,-4.5,6.15));
#20706=CARTESIAN_POINT('Origin',(0.9,-7.,8.));
#20707=CARTESIAN_POINT('',(1.2,-6.55758,7.58004221212127));
#20708=CARTESIAN_POINT('',(1.,-6.55758,7.58004221212127));
#20709=CARTESIAN_POINT('',(0.9,-6.55758,7.58004221212127));
#20710=CARTESIAN_POINT('',(1.2,-6.55758,8.41995778787873));
#20711=CARTESIAN_POINT('Origin',(1.2,-7.,8.));
#20712=CARTESIAN_POINT('',(1.,-6.55758,8.41995778787873));
#20713=CARTESIAN_POINT('',(0.9,-6.55758,8.41995778787873));
#20714=CARTESIAN_POINT('Origin',(1.,-7.,8.));
#20715=CARTESIAN_POINT('Origin',(0.9,-2.,8.));
#20716=CARTESIAN_POINT('',(1.2,-2.44242,8.41995778787873));
#20717=CARTESIAN_POINT('',(1.,-2.44242,8.41995778787873));
#20718=CARTESIAN_POINT('',(0.9,-2.44242,8.41995778787873));
#20719=CARTESIAN_POINT('',(1.2,-2.44242,7.58004221212127));
#20720=CARTESIAN_POINT('Origin',(1.2,-2.,8.));
#20721=CARTESIAN_POINT('',(1.,-2.44242,7.58004221212127));
#20722=CARTESIAN_POINT('',(0.9,-2.44242,7.58004221212127));
#20723=CARTESIAN_POINT('Origin',(1.,-2.,8.));
#20724=CARTESIAN_POINT('Origin',(1.2,-4.5,8.));
#20725=CARTESIAN_POINT('Origin',(1.2,-4.5,8.));
#20726=CARTESIAN_POINT('Origin',(1.2,-4.5,8.));
#20727=CARTESIAN_POINT('',(1.2,-4.5,9.02));
#20728=CARTESIAN_POINT('Origin',(1.2,-4.5,8.));
#20729=CARTESIAN_POINT('Origin',(1.,-4.5,8.));
#20730=CARTESIAN_POINT('Origin',(1.,-4.5,8.));
#20731=CARTESIAN_POINT('Origin',(1.,-4.5,8.));
#20732=CARTESIAN_POINT('Origin',(1.,-4.5,8.));
#20733=CARTESIAN_POINT('Origin',(1.,-4.5,8.));
#20734=CARTESIAN_POINT('',(1.,-4.5,9.02));
#20735=CARTESIAN_POINT('',(1.,-4.5,9.02));
#20736=CARTESIAN_POINT('Origin',(1.,-4.5,8.));
#20737=CARTESIAN_POINT('Origin',(1.,-4.5,8.));
#23521=UNCERTAINTY_MEASURE_WITH_UNIT(LENGTH_MEASURE(0.001),#23729,
'DISTANCE_ACCURACY_VALUE',
'Maximum model space distance between geometric entities at asserted c
onnectivities');
#23611=UNCERTAINTY_MEASURE_WITH_UNIT(LENGTH_MEASURE(0.001),#23729,
'DISTANCE_ACCURACY_VALUE',
'Maximum model space distance between geometric entities at asserted c
onnectivities');
#23638=(
GEOMETRIC_REPRESENTATION_CONTEXT(3)
GLOBAL_UNCERTAINTY_ASSIGNED_CONTEXT((#23521))
GLOBAL_UNIT_ASSIGNED_CONTEXT((#23729,#23731,#23732))
REPRESENTATION_CONTEXT('','3D')
);
#23728=(
GEOMETRIC_REPRESENTATION_CONTEXT(3)
GLOBAL_UNCERTAINTY_ASSIGNED_CONTEXT((#23611))
GLOBAL_UNIT_ASSIGNED_CONTEXT((#23729,#23731,#23732))
REPRESENTATION_CONTEXT('','3D')
);
#23729=(
LENGTH_UNIT()
NAMED_UNIT(*)
SI_UNIT(.CENTI.,.METRE.)
);
#23731=(
NAMED_UNIT(*)
PLANE_ANGLE_UNIT()
SI_UNIT($,.RADIAN.)
);
#23732=(
NAMED_UNIT(*)
SI_UNIT($,.STERADIAN.)
SOLID_ANGLE_UNIT()
);
#23759=SHAPE_DEFINITION_REPRESENTATION(#23875,#24138);
#23875=PRODUCT_DEFINITION_SHAPE('',$,#24255);
#24138=SHAPE_REPRESENTATION('',(#14119),#23638);
#24228=PRODUCT_DEFINITION_CONTEXT('part definition',#24578,'design');
#24255=PRODUCT_DEFINITION('Screw bearing keeper (3)',
'Screw bearing keeper (3)',#24371,#24228);
#24371=PRODUCT_DEFINITION_FORMATION('',$,#24606);
#24578=APPLICATION_CONTEXT(
'Core Data for Automotive Mechanical Design Process');
#24579=PRODUCT_CONTEXT('part definition',#24578,'mechanical');
#24606=PRODUCT('Screw bearing keeper (3)','Screw bearing keeper (3)',
'Screw bearing keeper (3)',(#24579));
#24766=COLOUR_RGB('Black',0.12,0.14,0.17);
#24767=FILL_AREA_STYLE_COLOUR('',#24766);
#24768=FILL_AREA_STYLE('',(#24767));
#24769=SURFACE_STYLE_FILL_AREA(#24768);
#24770=SURFACE_SIDE_STYLE('',(#24769));
#24771=SURFACE_STYLE_USAGE(.BOTH.,#24770);
#24772=PRESENTATION_STYLE_ASSIGNMENT((#24771));
ENDSEC;
END-ISO-10303-21;
